ISO-10303-21;
HEADER;
/* Generated by software containing ST-Developer
 * from STEP Tools, Inc. (www.steptools.com) 
 */

FILE_DESCRIPTION(
/* description */ ('Bell-crank linkage with push rods'),
/* implementation_level */ '2;1');

FILE_NAME(
/* name */ 'Plain link bushing (3).step',
/* time_stamp */ '2026-10-28T03:25:15-07:00',
/* author */ (''),
/* organization */ (''),
/* preprocessor_version */ 'ST-DEVELOPER v20.2',
/* originating_system */ 'Autodesk Translation Framework v15.17.0.0',
/* authorisation */ '');

FILE_SCHEMA (('AUTOMOTIVE_DESIGN { 1 0 10303 214 3 1 1 }'));
ENDSEC;

DATA;
#10=MECHANICAL_DESIGN_GEOMETRIC_PRESENTATION_REPRESENTATION('',(#648),#16678);
#532=SHAPE_REPRESENTATION_RELATIONSHIP('SRR','None',#16952,#586);
#586=ADVANCED_BREP_SHAPE_REPRESENTATION('',(#708),#16657);
#648=STYLED_ITEM('',(#17284),#708);
#708=MANIFOLD_SOLID_BREP('Body1',#8840);
#872=FACE_BOUND('',#2284,.T.);
#873=FACE_BOUND('',#2286,.T.);
#1157=PLANE('',#10229);
#1158=PLANE('',#10230);
#1612=FACE_OUTER_BOUND('',#2281,.T.);
#1613=FACE_OUTER_BOUND('',#2282,.T.);
#1614=FACE_OUTER_BOUND('',#2283,.T.);
#1615=FACE_OUTER_BOUND('',#2285,.T.);
#2281=EDGE_LOOP('',(#7443,#7444,#7445,#7446));
#2282=EDGE_LOOP('',(#7447,#7448,#7449,#7450));
#2283=EDGE_LOOP('',(#7451));
#2284=EDGE_LOOP('',(#7452));
#2285=EDGE_LOOP('',(#7453));
#2286=EDGE_LOOP('',(#7454));
#2906=LINE('',#15766,#3455);
#2907=LINE('',#15772,#3456);
#3455=VECTOR('',#12546,0.305);
#3456=VECTOR('',#12553,0.5);
#3983=CIRCLE('',#10224,0.305);
#3984=CIRCLE('',#10225,0.305);
#3985=CIRCLE('',#10227,0.5);
#3986=CIRCLE('',#10228,0.5);
#4626=VERTEX_POINT('',#15763);
#4627=VERTEX_POINT('',#15765);
#4628=VERTEX_POINT('',#15769);
#4629=VERTEX_POINT('',#15771);
#5599=EDGE_CURVE('',#4626,#4626,#3983,.T.);
#5600=EDGE_CURVE('',#4626,#4627,#2906,.T.);
#5601=EDGE_CURVE('',#4627,#4627,#3984,.T.);
#5602=EDGE_CURVE('',#4628,#4628,#3985,.T.);
#5603=EDGE_CURVE('',#4628,#4629,#2907,.T.);
#5604=EDGE_CURVE('',#4629,#4629,#3986,.T.);
#7443=ORIENTED_EDGE('',*,*,#5599,.F.);
#7444=ORIENTED_EDGE('',*,*,#5600,.T.);
#7445=ORIENTED_EDGE('',*,*,#5601,.T.);
#7446=ORIENTED_EDGE('',*,*,#5600,.F.);
#7447=ORIENTED_EDGE('',*,*,#5602,.F.);
#7448=ORIENTED_EDGE('',*,*,#5603,.T.);
#7449=ORIENTED_EDGE('',*,*,#5604,.T.);
#7450=ORIENTED_EDGE('',*,*,#5603,.F.);
#7451=ORIENTED_EDGE('',*,*,#5602,.T.);
#7452=ORIENTED_EDGE('',*,*,#5599,.T.);
#7453=ORIENTED_EDGE('',*,*,#5604,.F.);
#7454=ORIENTED_EDGE('',*,*,#5601,.F.);
#8208=CYLINDRICAL_SURFACE('',#10223,0.305);
#8209=CYLINDRICAL_SURFACE('',#10226,0.5);
#8637=ADVANCED_FACE('',(#1612),#8208,.F.);
#8638=ADVANCED_FACE('',(#1613),#8209,.T.);
#8639=ADVANCED_FACE('',(#1614,#872),#1157,.T.);
#8640=ADVANCED_FACE('',(#1615,#873),#1158,.F.);
#8840=CLOSED_SHELL('',(#8637,#8638,#8639,#8640));
#10222=AXIS2_PLACEMENT_3D('',#15761,#12540,#12541);
#10223=AXIS2_PLACEMENT_3D('',#15762,#12542,#12543);
#10224=AXIS2_PLACEMENT_3D('',#15764,#12544,#12545);
#10225=AXIS2_PLACEMENT_3D('',#15767,#12547,#12548);
#10226=AXIS2_PLACEMENT_3D('',#15768,#12549,#12550);
#10227=AXIS2_PLACEMENT_3D('',#15770,#12551,#12552);
#10228=AXIS2_PLACEMENT_3D('',#15773,#12554,#12555);
#10229=AXIS2_PLACEMENT_3D('',#15774,#12556,#12557);
#10230=AXIS2_PLACEMENT_3D('',#15775,#12558,#12559);
#12540=DIRECTION('axis',(0.,0.,1.));
#12541=DIRECTION('refdir',(1.,0.,0.));
#12542=DIRECTION('center_axis',(0.,0.,1.));
#12543=DIRECTION('ref_axis',(1.,0.,0.));
#12544=DIRECTION('center_axis',(0.,0.,-1.));
#12545=DIRECTION('ref_axis',(1.,0.,0.));
#12546=DIRECTION('',(0.,0.,-1.));
#12547=DIRECTION('center_axis',(0.,0.,-1.));
#12548=DIRECTION('ref_axis',(1.,0.,0.));
#12549=DIRECTION('center_axis',(0.,0.,1.));
#12550=DIRECTION('ref_axis',(1.,0.,0.));
#12551=DIRECTION('center_axis',(0.,0.,1.));
#12552=DIRECTION('ref_axis',(1.,0.,0.));
#12553=DIRECTION('',(0.,0.,-1.));
#12554=DIRECTION('center_axis',(0.,0.,1.));
#12555=DIRECTION('ref_axis',(1.,0.,0.));
#12556=DIRECTION('center_axis',(0.,0.,1.));
#12557=DIRECTION('ref_axis',(1.,0.,0.));
#12558=DIRECTION('center_axis',(0.,0.,1.));
#12559=DIRECTION('ref_axis',(1.,0.,0.));
#15761=CARTESIAN_POINT('',(0.,0.,0.));
#15762=CARTESIAN_POINT('Origin',(4.,12.,6.8));
#15763=CARTESIAN_POINT('',(3.695,12.,7.6));
#15764=CARTESIAN_POINT('Origin',(4.,12.,7.6));
#15765=CARTESIAN_POINT('',(3.695,12.,6.8));
#15766=CARTESIAN_POINT('',(3.695,12.,6.8));
#15767=CARTESIAN_POINT('Origin',(4.,12.,6.8));
#15768=CARTESIAN_POINT('Origin',(4.,12.,6.8));
#15769=CARTESIAN_POINT('',(3.5,12.,7.6));
#15770=CARTESIAN_POINT('Origin',(4.,12.,7.6));
#15771=CARTESIAN_POINT('',(3.5,12.,6.8));
#15772=CARTESIAN_POINT('',(3.5,12.,6.8));
#15773=CARTESIAN_POINT('Origin',(4.,12.,6.8));
#15774=CARTESIAN_POINT('Origin',(4.,12.,7.6));
#15775=CARTESIAN_POINT('Origin',(4.,12.,6.8));
#16593=UNCERTAINTY_MEASURE_WITH_UNIT(LENGTH_MEASURE(0.001),#16679,
'DISTANCE_ACCURACY_VALUE',
'Maximum model space distance between geometric entities at asserted c
onnectivities');
#16614=UNCERTAINTY_MEASURE_WITH_UNIT(LENGTH_MEASURE(0.001),#16679,
'DISTANCE_ACCURACY_VALUE',
'Maximum model space distance between geometric entities at asserted c
onnectivities');
#16657=(
GEOMETRIC_REPRESENTATION_CONTEXT(3)
GLOBAL_UNCERTAINTY_ASSIGNED_CONTEXT((#16593))
GLOBAL_UNIT_ASSIGNED_CONTEXT((#16679,#16681,#16682))
REPRESENTATION_CONTEXT('','3D')
);
#16678=(
GEOMETRIC_REPRESENTATION_CONTEXT(3)
GLOBAL_UNCERTAINTY_ASSIGNED_CONTEXT((#16614))
GLOBAL_UNIT_ASSIGNED_CONTEXT((#16679,#16681,#16682))
REPRESENTATION_CONTEXT('','3D')
);
#16679=(
LENGTH_UNIT()
NAMED_UNIT(*)
SI_UNIT(.CENTI.,.METRE.)
);
#16681=(
NAMED_UNIT(*)
PLANE_ANGLE_UNIT()
SI_UNIT($,.RADIAN.)
);
#16682=(
NAMED_UNIT(*)
SI_UNIT($,.STERADIAN.)
SOLID_ANGLE_UNIT()
);
#16725=SHAPE_DEFINITION_REPRESENTATION(#16796,#16952);
#16796=PRODUCT_DEFINITION_SHAPE('',$,#17016);
#16952=SHAPE_REPRESENTATION('',(#10222),#16657);
#16973=PRODUCT_DEFINITION_CONTEXT('part definition',#17164,'design');
#17016=PRODUCT_DEFINITION('Plain link bushing (3)',
'Plain link bushing (3)',#17079,#16973);
#17079=PRODUCT_DEFINITION_FORMATION('',$,#17208);
#17164=APPLICATION_CONTEXT(
'Core Data for Automotive Mechanical Design Process');
#17165=PRODUCT_CONTEXT('part definition',#17164,'mechanical');
#17208=PRODUCT('Plain link bushing (3)','Plain link bushing (3)',
'Plain link bushing (3)',(#17165));
#17278=COLOUR_RGB('Sky Blue',0.24,0.69,0.87);
#17279=FILL_AREA_STYLE_COLOUR('',#17278);
#17280=FILL_AREA_STYLE('',(#17279));
#17281=SURFACE_STYLE_FILL_AREA(#17280);
#17282=SURFACE_SIDE_STYLE('',(#17281));
#17283=SURFACE_STYLE_USAGE(.BOTH.,#17282);
#17284=PRESENTATION_STYLE_ASSIGNMENT((#17283));
ENDSEC;
END-ISO-10303-21;
